ISO-10303-21;
HEADER;
/* Generated by software containing ST-Developer
 * from STEP Tools, Inc. (www.steptools.com) 
 */

FILE_DESCRIPTION(
/* description */ ('PAT-065'),
/* implementation_level */ '2;1');

FILE_NAME(
/* name */ 'M5x14 Cap Screw.step',
/* time_stamp */ '2026-10-28T22:09:22-07:00',
/* author */ (''),
/* organization */ (''),
/* preprocessor_version */ 'ST-DEVELOPER v20.2',
/* originating_system */ 'Autodesk Translation Framework v15.17.0.0',
/* authorisation */ '');

FILE_SCHEMA (('AUTOMOTIVE_DESIGN { 1 0 10303 214 3 1 1 }'));
ENDSEC;

DATA;
#10=MECHANICAL_DESIGN_GEOMETRIC_PRESENTATION_REPRESENTATION('',(#167),#5502);
#126=CONICAL_SURFACE('',#3584,0.41,0.785398163397448);
#127=CONICAL_SURFACE('',#3588,0.26,0.463647609000806);
#147=SHAPE_REPRESENTATION_RELATIONSHIP('SRR','None',#5565,#157);
#157=ADVANCED_BREP_SHAPE_REPRESENTATION('',(#176),#5501);
#167=STYLED_ITEM('',(#5701),#176);
#176=MANIFOLD_SOLID_BREP('Body1',#3215);
#199=FACE_BOUND('',#695,.T.);
#200=FACE_BOUND('',#699,.T.);
#327=PLANE('',#3578);
#328=PLANE('',#3580);
#329=PLANE('',#3586);
#330=PLANE('',#3591);
#331=PLANE('',#3592);
#332=PLANE('',#3593);
#333=PLANE('',#3594);
#334=PLANE('',#3595);
#335=PLANE('',#3596);
#336=PLANE('',#3597);
#497=FACE_OUTER_BOUND('',#693,.T.);
#498=FACE_OUTER_BOUND('',#694,.T.);
#499=FACE_OUTER_BOUND('',#696,.T.);
#500=FACE_OUTER_BOUND('',#697,.T.);
#501=FACE_OUTER_BOUND('',#698,.T.);
#502=FACE_OUTER_BOUND('',#700,.T.);
#503=FACE_OUTER_BOUND('',#701,.T.);
#504=FACE_OUTER_BOUND('',#702,.T.);
#505=FACE_OUTER_BOUND('',#703,.T.);
#506=FACE_OUTER_BOUND('',#704,.T.);
#507=FACE_OUTER_BOUND('',#705,.T.);
#508=FACE_OUTER_BOUND('',#706,.T.);
#509=FACE_OUTER_BOUND('',#707,.T.);
#510=FACE_OUTER_BOUND('',#708,.T.);
#693=EDGE_LOOP('',(#2948));
#694=EDGE_LOOP('',(#2949));
#695=EDGE_LOOP('',(#2950,#2951,#2952,#2953,#2954,#2955));
#696=EDGE_LOOP('',(#2956,#2957,#2958,#2959));
#697=EDGE_LOOP('',(#2960,#2961,#2962,#2963));
#698=EDGE_LOOP('',(#2964));
#699=EDGE_LOOP('',(#2965));
#700=EDGE_LOOP('',(#2966,#2967,#2968,#2969));
#701=EDGE_LOOP('',(#2970,#2971,#2972,#2973));
#702=EDGE_LOOP('',(#2974,#2975,#2976,#2977));
#703=EDGE_LOOP('',(#2978,#2979,#2980,#2981));
#704=EDGE_LOOP('',(#2982,#2983,#2984,#2985));
#705=EDGE_LOOP('',(#2986,#2987,#2988,#2989));
#706=EDGE_LOOP('',(#2990,#2991,#2992,#2993));
#707=EDGE_LOOP('',(#2994,#2995,#2996,#2997));
#708=EDGE_LOOP('',(#2998,#2999,#3000,#3001,#3002,#3003));
#1018=LINE('',#5405,#1349);
#1019=LINE('',#5407,#1350);
#1020=LINE('',#5409,#1351);
#1021=LINE('',#5411,#1352);
#1022=LINE('',#5413,#1353);
#1023=LINE('',#5414,#1354);
#1024=LINE('',#5418,#1355);
#1025=LINE('',#5422,#1356);
#1026=LINE('',#5429,#1357);
#1027=LINE('',#5431,#1358);
#1028=LINE('',#5435,#1359);
#1029=LINE('',#5436,#1360);
#1030=LINE('',#5437,#1361);
#1031=LINE('',#5440,#1362);
#1032=LINE('',#5441,#1363);
#1033=LINE('',#5444,#1364);
#1034=LINE('',#5445,#1365);
#1035=LINE('',#5448,#1366);
#1036=LINE('',#5449,#1367);
#1037=LINE('',#5452,#1368);
#1038=LINE('',#5453,#1369);
#1039=LINE('',#5455,#1370);
#1349=VECTOR('',#4437,1.);
#1350=VECTOR('',#4438,1.);
#1351=VECTOR('',#4439,1.);
#1352=VECTOR('',#4440,1.);
#1353=VECTOR('',#4441,1.);
#1354=VECTOR('',#4442,1.);
#1355=VECTOR('',#4447,0.425);
#1356=VECTOR('',#4452,0.41);
#1357=VECTOR('',#4461,0.26);
#1358=VECTOR('',#4464,0.25);
#1359=VECTOR('',#4467,1.);
#1360=VECTOR('',#4468,1.);
#1361=VECTOR('',#4469,1.);
#1362=VECTOR('',#4472,1.);
#1363=VECTOR('',#4473,1.);
#1364=VECTOR('',#4476,1.);
#1365=VECTOR('',#4477,1.);
#1366=VECTOR('',#4480,1.);
#1367=VECTOR('',#4481,1.);
#1368=VECTOR('',#4484,1.);
#1369=VECTOR('',#4485,1.);
#1370=VECTOR('',#4488,1.);
#1438=CIRCLE('',#3579,0.425);
#1439=CIRCLE('',#3581,0.24505);
#1440=CIRCLE('',#3583,0.425);
#1441=CIRCLE('',#3585,0.395);
#1442=CIRCLE('',#3587,0.27);
#1443=CIRCLE('',#3589,0.24505);
#1708=VERTEX_POINT('',#5398);
#1709=VERTEX_POINT('',#5401);
#1710=VERTEX_POINT('',#5403);
#1711=VERTEX_POINT('',#5404);
#1712=VERTEX_POINT('',#5406);
#1713=VERTEX_POINT('',#5408);
#1714=VERTEX_POINT('',#5410);
#1715=VERTEX_POINT('',#5412);
#1716=VERTEX_POINT('',#5416);
#1717=VERTEX_POINT('',#5420);
#1718=VERTEX_POINT('',#5424);
#1719=VERTEX_POINT('',#5427);
#1720=VERTEX_POINT('',#5433);
#1721=VERTEX_POINT('',#5434);
#1722=VERTEX_POINT('',#5439);
#1723=VERTEX_POINT('',#5443);
#1724=VERTEX_POINT('',#5447);
#1725=VERTEX_POINT('',#5451);
#2124=EDGE_CURVE('',#1708,#1708,#1438,.T.);
#2125=EDGE_CURVE('',#1709,#1709,#1439,.T.);
#2126=EDGE_CURVE('',#1710,#1711,#1018,.T.);
#2127=EDGE_CURVE('',#1712,#1710,#1019,.T.);
#2128=EDGE_CURVE('',#1713,#1712,#1020,.T.);
#2129=EDGE_CURVE('',#1714,#1713,#1021,.T.);
#2130=EDGE_CURVE('',#1715,#1714,#1022,.T.);
#2131=EDGE_CURVE('',#1711,#1715,#1023,.T.);
#2132=EDGE_CURVE('',#1716,#1716,#1440,.T.);
#2133=EDGE_CURVE('',#1716,#1708,#1024,.T.);
#2134=EDGE_CURVE('',#1717,#1717,#1441,.T.);
#2135=EDGE_CURVE('',#1717,#1716,#1025,.T.);
#2136=EDGE_CURVE('',#1718,#1718,#1442,.T.);
#2137=EDGE_CURVE('',#1719,#1719,#1443,.F.);
#2138=EDGE_CURVE('',#1719,#1718,#1026,.T.);
#2139=EDGE_CURVE('',#1709,#1719,#1027,.T.);
#2140=EDGE_CURVE('',#1720,#1721,#1028,.T.);
#2141=EDGE_CURVE('',#1721,#1710,#1029,.T.);
#2142=EDGE_CURVE('',#1720,#1711,#1030,.T.);
#2143=EDGE_CURVE('',#1721,#1722,#1031,.T.);
#2144=EDGE_CURVE('',#1722,#1712,#1032,.T.);
#2145=EDGE_CURVE('',#1722,#1723,#1033,.T.);
#2146=EDGE_CURVE('',#1723,#1713,#1034,.T.);
#2147=EDGE_CURVE('',#1723,#1724,#1035,.T.);
#2148=EDGE_CURVE('',#1724,#1714,#1036,.T.);
#2149=EDGE_CURVE('',#1724,#1725,#1037,.T.);
#2150=EDGE_CURVE('',#1725,#1715,#1038,.T.);
#2151=EDGE_CURVE('',#1725,#1720,#1039,.T.);
#2948=ORIENTED_EDGE('',*,*,#2124,.F.);
#2949=ORIENTED_EDGE('',*,*,#2125,.F.);
#2950=ORIENTED_EDGE('',*,*,#2126,.F.);
#2951=ORIENTED_EDGE('',*,*,#2127,.F.);
#2952=ORIENTED_EDGE('',*,*,#2128,.F.);
#2953=ORIENTED_EDGE('',*,*,#2129,.F.);
#2954=ORIENTED_EDGE('',*,*,#2130,.F.);
#2955=ORIENTED_EDGE('',*,*,#2131,.F.);
#2956=ORIENTED_EDGE('',*,*,#2132,.F.);
#2957=ORIENTED_EDGE('',*,*,#2133,.T.);
#2958=ORIENTED_EDGE('',*,*,#2124,.T.);
#2959=ORIENTED_EDGE('',*,*,#2133,.F.);
#2960=ORIENTED_EDGE('',*,*,#2134,.F.);
#2961=ORIENTED_EDGE('',*,*,#2135,.T.);
#2962=ORIENTED_EDGE('',*,*,#2132,.T.);
#2963=ORIENTED_EDGE('',*,*,#2135,.F.);
#2964=ORIENTED_EDGE('',*,*,#2134,.T.);
#2965=ORIENTED_EDGE('',*,*,#2136,.F.);
#2966=ORIENTED_EDGE('',*,*,#2137,.F.);
#2967=ORIENTED_EDGE('',*,*,#2138,.T.);
#2968=ORIENTED_EDGE('',*,*,#2136,.T.);
#2969=ORIENTED_EDGE('',*,*,#2138,.F.);
#2970=ORIENTED_EDGE('',*,*,#2125,.T.);
#2971=ORIENTED_EDGE('',*,*,#2139,.T.);
#2972=ORIENTED_EDGE('',*,*,#2137,.T.);
#2973=ORIENTED_EDGE('',*,*,#2139,.F.);
#2974=ORIENTED_EDGE('',*,*,#2140,.T.);
#2975=ORIENTED_EDGE('',*,*,#2141,.T.);
#2976=ORIENTED_EDGE('',*,*,#2126,.T.);
#2977=ORIENTED_EDGE('',*,*,#2142,.F.);
#2978=ORIENTED_EDGE('',*,*,#2143,.T.);
#2979=ORIENTED_EDGE('',*,*,#2144,.T.);
#2980=ORIENTED_EDGE('',*,*,#2127,.T.);
#2981=ORIENTED_EDGE('',*,*,#2141,.F.);
#2982=ORIENTED_EDGE('',*,*,#2145,.T.);
#2983=ORIENTED_EDGE('',*,*,#2146,.T.);
#2984=ORIENTED_EDGE('',*,*,#2128,.T.);
#2985=ORIENTED_EDGE('',*,*,#2144,.F.);
#2986=ORIENTED_EDGE('',*,*,#2147,.T.);
#2987=ORIENTED_EDGE('',*,*,#2148,.T.);
#2988=ORIENTED_EDGE('',*,*,#2129,.T.);
#2989=ORIENTED_EDGE('',*,*,#2146,.F.);
#2990=ORIENTED_EDGE('',*,*,#2149,.T.);
#2991=ORIENTED_EDGE('',*,*,#2150,.T.);
#2992=ORIENTED_EDGE('',*,*,#2130,.T.);
#2993=ORIENTED_EDGE('',*,*,#2148,.F.);
#2994=ORIENTED_EDGE('',*,*,#2151,.T.);
#2995=ORIENTED_EDGE('',*,*,#2142,.T.);
#2996=ORIENTED_EDGE('',*,*,#2131,.T.);
#2997=ORIENTED_EDGE('',*,*,#2150,.F.);
#2998=ORIENTED_EDGE('',*,*,#2151,.F.);
#2999=ORIENTED_EDGE('',*,*,#2149,.F.);
#3000=ORIENTED_EDGE('',*,*,#2147,.F.);
#3001=ORIENTED_EDGE('',*,*,#2145,.F.);
#3002=ORIENTED_EDGE('',*,*,#2143,.F.);
#3003=ORIENTED_EDGE('',*,*,#2140,.F.);
#3029=CYLINDRICAL_SURFACE('',#3582,0.425);
#3030=CYLINDRICAL_SURFACE('',#3590,0.24505);
#3191=ADVANCED_FACE('',(#497),#327,.T.);
#3192=ADVANCED_FACE('',(#498,#199),#328,.F.);
#3193=ADVANCED_FACE('',(#499),#3029,.T.);
#3194=ADVANCED_FACE('',(#500),#126,.T.);
#3195=ADVANCED_FACE('',(#501,#200),#329,.T.);
#3196=ADVANCED_FACE('',(#502),#127,.T.);
#3197=ADVANCED_FACE('',(#503),#3030,.T.);
#3198=ADVANCED_FACE('',(#504),#330,.F.);
#3199=ADVANCED_FACE('',(#505),#331,.F.);
#3200=ADVANCED_FACE('',(#506),#332,.F.);
#3201=ADVANCED_FACE('',(#507),#333,.F.);
#3202=ADVANCED_FACE('',(#508),#334,.F.);
#3203=ADVANCED_FACE('',(#509),#335,.F.);
#3204=ADVANCED_FACE('',(#510),#336,.F.);
#3215=CLOSED_SHELL('',(#3191,#3192,#3193,#3194,#3195,#3196,#3197,#3198,
#3199,#3200,#3201,#3202,#3203,#3204));
#3577=AXIS2_PLACEMENT_3D('',#5396,#4427,#4428);
#3578=AXIS2_PLACEMENT_3D('',#5397,#4429,#4430);
#3579=AXIS2_PLACEMENT_3D('',#5399,#4431,#4432);
#3580=AXIS2_PLACEMENT_3D('',#5400,#4433,#4434);
#3581=AXIS2_PLACEMENT_3D('',#5402,#4435,#4436);
#3582=AXIS2_PLACEMENT_3D('',#5415,#4443,#4444);
#3583=AXIS2_PLACEMENT_3D('',#5417,#4445,#4446);
#3584=AXIS2_PLACEMENT_3D('',#5419,#4448,#4449);
#3585=AXIS2_PLACEMENT_3D('',#5421,#4450,#4451);
#3586=AXIS2_PLACEMENT_3D('',#5423,#4453,#4454);
#3587=AXIS2_PLACEMENT_3D('',#5425,#4455,#4456);
#3588=AXIS2_PLACEMENT_3D('',#5426,#4457,#4458);
#3589=AXIS2_PLACEMENT_3D('',#5428,#4459,#4460);
#3590=AXIS2_PLACEMENT_3D('',#5430,#4462,#4463);
#3591=AXIS2_PLACEMENT_3D('',#5432,#4465,#4466);
#3592=AXIS2_PLACEMENT_3D('',#5438,#4470,#4471);
#3593=AXIS2_PLACEMENT_3D('',#5442,#4474,#4475);
#3594=AXIS2_PLACEMENT_3D('',#5446,#4478,#4479);
#3595=AXIS2_PLACEMENT_3D('',#5450,#4482,#4483);
#3596=AXIS2_PLACEMENT_3D('',#5454,#4486,#4487);
#3597=AXIS2_PLACEMENT_3D('',#5456,#4489,#4490);
#4427=DIRECTION('axis',(0.,0.,1.));
#4428=DIRECTION('refdir',(1.,0.,0.));
#4429=DIRECTION('center_axis',(0.,1.,0.));
#4430=DIRECTION('ref_axis',(1.,0.,0.));
#4431=DIRECTION('center_axis',(0.,-1.,0.));
#4432=DIRECTION('ref_axis',(1.,0.,0.));
#4433=DIRECTION('center_axis',(0.,1.,0.));
#4434=DIRECTION('ref_axis',(1.,0.,0.));
#4435=DIRECTION('center_axis',(0.,1.,0.));
#4436=DIRECTION('ref_axis',(1.,0.,0.));
#4437=DIRECTION('',(0.5,0.,0.866025403784439));
#4438=DIRECTION('',(1.,0.,1.20185167898973E-16));
#4439=DIRECTION('',(0.5,0.,-0.866025403784439));
#4440=DIRECTION('',(-0.5,0.,-0.866025403784439));
#4441=DIRECTION('',(-1.,0.,-2.40370335797945E-16));
#4442=DIRECTION('',(-0.5,0.,0.866025403784439));
#4443=DIRECTION('center_axis',(0.,-1.,0.));
#4444=DIRECTION('ref_axis',(1.,0.,0.));
#4445=DIRECTION('center_axis',(0.,-1.,0.));
#4446=DIRECTION('ref_axis',(1.,0.,0.));
#4447=DIRECTION('',(0.,1.,0.));
#4448=DIRECTION('center_axis',(0.,1.,0.));
#4449=DIRECTION('ref_axis',(1.,0.,0.));
#4450=DIRECTION('center_axis',(0.,-1.,0.));
#4451=DIRECTION('ref_axis',(1.,0.,0.));
#4452=DIRECTION('',(-0.707106781186547,0.707106781186548,-8.65956056235493E-17));
#4453=DIRECTION('center_axis',(0.,-1.,0.));
#4454=DIRECTION('ref_axis',(0.,0.,-1.));
#4455=DIRECTION('center_axis',(0.,-1.,0.));
#4456=DIRECTION('ref_axis',(1.,0.,0.));
#4457=DIRECTION('center_axis',(0.,1.,0.));
#4458=DIRECTION('ref_axis',(1.,0.,0.));
#4459=DIRECTION('center_axis',(0.,1.,0.));
#4460=DIRECTION('ref_axis',(1.,0.,0.));
#4461=DIRECTION('',(-0.447213595499958,0.894427190999916,-5.47678698264203E-17));
#4462=DIRECTION('center_axis',(0.,-1.,0.));
#4463=DIRECTION('ref_axis',(1.,0.,0.));
#4464=DIRECTION('',(0.,1.,0.));
#4465=DIRECTION('center_axis',(0.866025403784439,0.,-0.5));
#4466=DIRECTION('ref_axis',(0.5,0.,0.866025403784439));
#4467=DIRECTION('',(-0.5,0.,-0.866025403784439));
#4468=DIRECTION('',(0.,-1.,0.));
#4469=DIRECTION('',(0.,-1.,0.));
#4470=DIRECTION('center_axis',(1.20185167898973E-16,0.,-1.));
#4471=DIRECTION('ref_axis',(1.,0.,1.20185167898973E-16));
#4472=DIRECTION('',(-1.,0.,-1.20185167898973E-16));
#4473=DIRECTION('',(0.,-1.,0.));
#4474=DIRECTION('center_axis',(-0.866025403784439,0.,-0.5));
#4475=DIRECTION('ref_axis',(0.5,0.,-0.866025403784439));
#4476=DIRECTION('',(-0.5,0.,0.866025403784439));
#4477=DIRECTION('',(0.,-1.,0.));
#4478=DIRECTION('center_axis',(-0.866025403784439,0.,0.5));
#4479=DIRECTION('ref_axis',(-0.5,0.,-0.866025403784439));
#4480=DIRECTION('',(0.5,0.,0.866025403784439));
#4481=DIRECTION('',(0.,-1.,0.));
#4482=DIRECTION('center_axis',(-2.40370335797945E-16,0.,1.));
#4483=DIRECTION('ref_axis',(-1.,0.,-2.40370335797945E-16));
#4484=DIRECTION('',(1.,0.,2.40370335797945E-16));
#4485=DIRECTION('',(0.,-1.,0.));
#4486=DIRECTION('center_axis',(0.866025403784439,0.,0.5));
#4487=DIRECTION('ref_axis',(-0.5,0.,0.866025403784439));
#4488=DIRECTION('',(0.5,0.,-0.866025403784439));
#4489=DIRECTION('center_axis',(0.,1.,0.));
#4490=DIRECTION('ref_axis',(1.,0.,0.));
#5396=CARTESIAN_POINT('',(0.,0.,0.));
#5397=CARTESIAN_POINT('Origin',(0.,0.2,0.));
#5398=CARTESIAN_POINT('',(-0.425,0.2,-5.20474889637625E-17));
#5399=CARTESIAN_POINT('Origin',(0.,0.2,0.));
#5400=CARTESIAN_POINT('Origin',(0.,-0.8,0.));
#5401=CARTESIAN_POINT('',(-0.24505,-0.8,3.00099698131059E-17));
#5402=CARTESIAN_POINT('Origin',(0.,-0.8,0.));
#5403=CARTESIAN_POINT('',(0.115470053837925,-0.8,-0.2));
#5404=CARTESIAN_POINT('',(0.23094010767585,-0.8,0.));
#5405=CARTESIAN_POINT('',(0.23094010767585,-0.8,0.));
#5406=CARTESIAN_POINT('',(-0.115470053837925,-0.8,-0.2));
#5407=CARTESIAN_POINT('',(0.115470053837925,-0.8,-0.2));
#5408=CARTESIAN_POINT('',(-0.23094010767585,-0.8,-2.77555756156289E-17));
#5409=CARTESIAN_POINT('',(-0.115470053837925,-0.8,-0.2));
#5410=CARTESIAN_POINT('',(-0.115470053837925,-0.8,0.2));
#5411=CARTESIAN_POINT('',(-0.23094010767585,-0.8,-2.82820063659975E-17));
#5412=CARTESIAN_POINT('',(0.115470053837925,-0.8,0.2));
#5413=CARTESIAN_POINT('',(-0.115470053837925,-0.8,0.2));
#5414=CARTESIAN_POINT('',(0.115470053837925,-0.8,0.2));
#5415=CARTESIAN_POINT('Origin',(0.,0.24,0.));
#5416=CARTESIAN_POINT('',(-0.425,0.0299999999999998,-5.20474889637625E-17));
#5417=CARTESIAN_POINT('Origin',(0.,0.0299999999999998,0.));
#5418=CARTESIAN_POINT('',(-0.425,0.24,-5.20474889637625E-17));
#5419=CARTESIAN_POINT('Origin',(0.,0.0150000000000001,0.));
#5420=CARTESIAN_POINT('',(-0.395,4.85722573273506E-17,-4.83735485663204E-17));
#5421=CARTESIAN_POINT('Origin',(0.,0.,0.));
#5422=CARTESIAN_POINT('',(-0.41,0.0150000000000001,-5.02105187650415E-17));
#5423=CARTESIAN_POINT('Origin',(0.27,0.,0.));
#5424=CARTESIAN_POINT('',(-0.27,0.,-3.30654635769785E-17));
#5425=CARTESIAN_POINT('Origin',(0.,0.,0.));
#5426=CARTESIAN_POINT('Origin',(0.,-0.02,0.));
#5427=CARTESIAN_POINT('',(-0.24505,-0.0498999999999999,3.00099698131059E-17));
#5428=CARTESIAN_POINT('Origin',(0.,-0.0498999999999999,0.));
#5429=CARTESIAN_POINT('',(-0.26,-0.02,-3.18408167778312E-17));
#5430=CARTESIAN_POINT('Origin',(0.,-0.995,0.));
#5431=CARTESIAN_POINT('',(-0.24505,-0.995,-3.00099698131059E-17));
#5432=CARTESIAN_POINT('Origin',(0.115470053837925,-0.5,-0.2));
#5433=CARTESIAN_POINT('',(0.23094010767585,-0.5,0.));
#5434=CARTESIAN_POINT('',(0.115470053837925,-0.5,-0.2));
#5435=CARTESIAN_POINT('',(0.23094010767585,-0.5,0.));
#5436=CARTESIAN_POINT('',(0.115470053837925,-0.5,-0.2));
#5437=CARTESIAN_POINT('',(0.23094010767585,-0.5,0.));
#5438=CARTESIAN_POINT('Origin',(-0.115470053837925,-0.5,-0.2));
#5439=CARTESIAN_POINT('',(-0.115470053837925,-0.5,-0.2));
#5440=CARTESIAN_POINT('',(0.115470053837925,-0.5,-0.2));
#5441=CARTESIAN_POINT('',(-0.115470053837925,-0.5,-0.2));
#5442=CARTESIAN_POINT('Origin',(-0.23094010767585,-0.5,-2.77555756156289E-17));
#5443=CARTESIAN_POINT('',(-0.23094010767585,-0.5,-2.82820063659975E-17));
#5444=CARTESIAN_POINT('',(-0.115470053837925,-0.5,-0.2));
#5445=CARTESIAN_POINT('',(-0.23094010767585,-0.5,-2.82820063659975E-17));
#5446=CARTESIAN_POINT('Origin',(-0.115470053837925,-0.5,0.2));
#5447=CARTESIAN_POINT('',(-0.115470053837925,-0.5,0.2));
#5448=CARTESIAN_POINT('',(-0.23094010767585,-0.5,-2.82820063659975E-17));
#5449=CARTESIAN_POINT('',(-0.115470053837925,-0.5,0.2));
#5450=CARTESIAN_POINT('Origin',(0.115470053837925,-0.5,0.2));
#5451=CARTESIAN_POINT('',(0.115470053837925,-0.5,0.2));
#5452=CARTESIAN_POINT('',(-0.115470053837925,-0.5,0.2));
#5453=CARTESIAN_POINT('',(0.115470053837925,-0.5,0.2));
#5454=CARTESIAN_POINT('Origin',(0.23094010767585,-0.5,0.));
#5455=CARTESIAN_POINT('',(0.115470053837925,-0.5,0.2));
#5456=CARTESIAN_POINT('Origin',(0.,-0.5,0.));
#5488=UNCERTAINTY_MEASURE_WITH_UNIT(LENGTH_MEASURE(0.001),#5503,
'DISTANCE_ACCURACY_VALUE',
'Maximum model space distance between geometric entities at asserted c
onnectivities');
#5489=UNCERTAINTY_MEASURE_WITH_UNIT(LENGTH_MEASURE(0.001),#5503,
'DISTANCE_ACCURACY_VALUE',
'Maximum model space distance between geometric entities at asserted c
onnectivities');
#5501=(
GEOMETRIC_REPRESENTATION_CONTEXT(3)
GLOBAL_UNCERTAINTY_ASSIGNED_CONTEXT((#5488))
GLOBAL_UNIT_ASSIGNED_CONTEXT((#5503,#5505,#5506))
REPRESENTATION_CONTEXT('','3D')
);
#5502=(
GEOMETRIC_REPRESENTATION_CONTEXT(3)
GLOBAL_UNCERTAINTY_ASSIGNED_CONTEXT((#5489))
GLOBAL_UNIT_ASSIGNED_CONTEXT((#5503,#5505,#5506))
REPRESENTATION_CONTEXT('','3D')
);
#5503=(
LENGTH_UNIT()
NAMED_UNIT(*)
SI_UNIT(.CENTI.,.METRE.)
);
#5505=(
NAMED_UNIT(*)
PLANE_ANGLE_UNIT()
SI_UNIT($,.RADIAN.)
);
#5506=(
NAMED_UNIT(*)
SI_UNIT($,.STERADIAN.)
SOLID_ANGLE_UNIT()
);
#5518=SHAPE_DEFINITION_REPRESENTATION(#5533,#5565);
#5533=PRODUCT_DEFINITION_SHAPE('',$,#5578);
#5565=SHAPE_REPRESENTATION('',(#3577),#5501);
#5566=PRODUCT_DEFINITION_CONTEXT('part definition',#5604,'design');
#5578=PRODUCT_DEFINITION('M5x14 Cap Screw','M5x14 Cap Screw',
#5590,#5566);
#5590=PRODUCT_DEFINITION_FORMATION('',$,#5617);
#5604=APPLICATION_CONTEXT(
'Core Data for Automotive Mechanical Design Process');
#5605=PRODUCT_CONTEXT('part definition',#5604,'mechanical');
#5617=PRODUCT('M5x14 Cap Screw','M5x14 Cap Screw',
'M5x14 Cap Screw',(#5605));
#5695=COLOUR_RGB('Black',0.12,0.14,0.17);
#5696=FILL_AREA_STYLE_COLOUR('',#5695);
#5697=FILL_AREA_STYLE('',(#5696));
#5698=SURFACE_STYLE_FILL_AREA(#5697);
#5699=SURFACE_SIDE_STYLE('',(#5698));
#5700=SURFACE_STYLE_USAGE(.BOTH.,#5699);
#5701=PRESENTATION_STYLE_ASSIGNMENT((#5700));
ENDSEC;
END-ISO-10303-21;
